ISO-10303-21;
HEADER;
/* Generated by software containing ST-Developer
 * from STEP Tools, Inc. (www.steptools.com) 
 */

FILE_DESCRIPTION(
/* description */ ('Hand-operated arbor press'),
/* implementation_level */ '2;1');

FILE_NAME(
/* name */ 'Cap Screw - M5x20.step',
/* time_stamp */ '2026-10-28T03:25:25-07:00',
/* author */ (''),
/* organization */ (''),
/* preprocessor_version */ 'ST-DEVELOPER v20.2',
/* originating_system */ 'Autodesk Translation Framework v15.17.0.0',
/* authorisation */ '');

FILE_SCHEMA (('AUTOMOTIVE_DESIGN { 1 0 10303 214 3 1 1 }'));
ENDSEC;

DATA;
#10=MECHANICAL_DESIGN_GEOMETRIC_PRESENTATION_REPRESENTATION('',(#601),#32751);
#473=ORIENTED_CLOSED_SHELL('',*,#12499,.F.);
#477=CONICAL_SURFACE('',#13391,0.4,0.785398163397448);
#478=CONICAL_SURFACE('',#13395,0.41,0.785398163397448);
#479=CONICAL_SURFACE('',#13399,0.26,0.463647609000806);
#480=CONICAL_SURFACE('',#13403,0.225,0.785398163397448);
#498=BREP_WITH_VOIDS('Body1',#12498,(#473));
#517=SHAPE_REPRESENTATION_RELATIONSHIP('SRR','None',#32946,#559);
#559=ADVANCED_BREP_SHAPE_REPRESENTATION('',(#498),#32720);
#601=STYLED_ITEM('',(#33249),#498);
#801=FACE_BOUND('',#2302,.T.);
#966=PLANE('',#13389);
#967=PLANE('',#13397);
#968=PLANE('',#13405);
#969=PLANE('',#13406);
#970=PLANE('',#13407);
#971=PLANE('',#13408);
#972=PLANE('',#13409);
#973=PLANE('',#13410);
#974=PLANE('',#13411);
#975=PLANE('',#13412);
#976=PLANE('',#13413);
#1495=FACE_OUTER_BOUND('',#2297,.T.);
#1496=FACE_OUTER_BOUND('',#2298,.T.);
#1497=FACE_OUTER_BOUND('',#2299,.T.);
#1498=FACE_OUTER_BOUND('',#2300,.T.);
#1499=FACE_OUTER_BOUND('',#2301,.T.);
#1500=FACE_OUTER_BOUND('',#2303,.T.);
#1501=FACE_OUTER_BOUND('',#2304,.T.);
#1502=FACE_OUTER_BOUND('',#2305,.T.);
#1503=FACE_OUTER_BOUND('',#2306,.T.);
#1504=FACE_OUTER_BOUND('',#2307,.T.);
#1505=FACE_OUTER_BOUND('',#2308,.T.);
#1506=FACE_OUTER_BOUND('',#2309,.T.);
#1507=FACE_OUTER_BOUND('',#2310,.T.);
#1508=FACE_OUTER_BOUND('',#2311,.T.);
#1509=FACE_OUTER_BOUND('',#2312,.T.);
#1510=FACE_OUTER_BOUND('',#2313,.T.);
#1511=FACE_OUTER_BOUND('',#2314,.T.);
#2297=EDGE_LOOP('',(#9278));
#2298=EDGE_LOOP('',(#9279,#9280,#9281,#9282));
#2299=EDGE_LOOP('',(#9283,#9284,#9285,#9286));
#2300=EDGE_LOOP('',(#9287,#9288,#9289,#9290));
#2301=EDGE_LOOP('',(#9291));
#2302=EDGE_LOOP('',(#9292));
#2303=EDGE_LOOP('',(#9293,#9294,#9295,#9296));
#2304=EDGE_LOOP('',(#9297,#9298,#9299,#9300));
#2305=EDGE_LOOP('',(#9301,#9302,#9303,#9304));
#2306=EDGE_LOOP('',(#9305));
#2307=EDGE_LOOP('',(#9306,#9307,#9308,#9309));
#2308=EDGE_LOOP('',(#9310,#9311,#9312,#9313));
#2309=EDGE_LOOP('',(#9314,#9315,#9316,#9317));
#2310=EDGE_LOOP('',(#9318,#9319,#9320,#9321));
#2311=EDGE_LOOP('',(#9322,#9323,#9324,#9325));
#2312=EDGE_LOOP('',(#9326,#9327,#9328,#9329));
#2313=EDGE_LOOP('',(#9330,#9331,#9332,#9333,#9334,#9335));
#2314=EDGE_LOOP('',(#9336,#9337,#9338,#9339,#9340,#9341));
#3131=LINE('',#18659,#4302);
#3132=LINE('',#18663,#4303);
#3133=LINE('',#18667,#4304);
#3134=LINE('',#18674,#4305);
#3135=LINE('',#18678,#4306);
#3136=LINE('',#18682,#4307);
#3137=LINE('',#18687,#4308);
#3138=LINE('',#18689,#4309);
#3139=LINE('',#18691,#4310);
#3140=LINE('',#18692,#4311);
#3141=LINE('',#18695,#4312);
#3142=LINE('',#18697,#4313);
#3143=LINE('',#18698,#4314);
#3144=LINE('',#18701,#4315);
#3145=LINE('',#18703,#4316);
#3146=LINE('',#18704,#4317);
#3147=LINE('',#18707,#4318);
#3148=LINE('',#18709,#4319);
#3149=LINE('',#18710,#4320);
#3150=LINE('',#18713,#4321);
#3151=LINE('',#18715,#4322);
#3152=LINE('',#18716,#4323);
#3153=LINE('',#18718,#4324);
#3154=LINE('',#18719,#4325);
#4302=VECTOR('',#15250,0.4);
#4303=VECTOR('',#15255,0.425);
#4304=VECTOR('',#15260,0.41);
#4305=VECTOR('',#15269,0.26);
#4306=VECTOR('',#15274,0.25);
#4307=VECTOR('',#15279,0.225);
#4308=VECTOR('',#15284,1.);
#4309=VECTOR('',#15285,1.);
#4310=VECTOR('',#15286,1.);
#4311=VECTOR('',#15287,1.);
#4312=VECTOR('',#15290,1.);
#4313=VECTOR('',#15291,1.);
#4314=VECTOR('',#15292,1.);
#4315=VECTOR('',#15295,1.);
#4316=VECTOR('',#15296,1.);
#4317=VECTOR('',#15297,1.);
#4318=VECTOR('',#15300,1.);
#4319=VECTOR('',#15301,1.);
#4320=VECTOR('',#15302,1.);
#4321=VECTOR('',#15305,1.);
#4322=VECTOR('',#15306,1.);
#4323=VECTOR('',#15307,1.);
#4324=VECTOR('',#15310,1.);
#4325=VECTOR('',#15311,1.);
#5336=CIRCLE('',#13390,0.375);
#5337=CIRCLE('',#13392,0.425);
#5338=CIRCLE('',#13394,0.425);
#5339=CIRCLE('',#13396,0.395);
#5340=CIRCLE('',#13398,0.27);
#5341=CIRCLE('',#13400,0.24505);
#5342=CIRCLE('',#13402,0.24505);
#5343=CIRCLE('',#13404,0.2);
#5874=VERTEX_POINT('',#18654);
#5875=VERTEX_POINT('',#18657);
#5876=VERTEX_POINT('',#18661);
#5877=VERTEX_POINT('',#18665);
#5878=VERTEX_POINT('',#18669);
#5879=VERTEX_POINT('',#18672);
#5880=VERTEX_POINT('',#18676);
#5881=VERTEX_POINT('',#18680);
#5882=VERTEX_POINT('',#18685);
#5883=VERTEX_POINT('',#18686);
#5884=VERTEX_POINT('',#18688);
#5885=VERTEX_POINT('',#18690);
#5886=VERTEX_POINT('',#18694);
#5887=VERTEX_POINT('',#18696);
#5888=VERTEX_POINT('',#18700);
#5889=VERTEX_POINT('',#18702);
#5890=VERTEX_POINT('',#18706);
#5891=VERTEX_POINT('',#18708);
#5892=VERTEX_POINT('',#18712);
#5893=VERTEX_POINT('',#18714);
#7142=EDGE_CURVE('',#5874,#5874,#5336,.T.);
#7143=EDGE_CURVE('',#5875,#5875,#5337,.T.);
#7144=EDGE_CURVE('',#5875,#5874,#3131,.T.);
#7145=EDGE_CURVE('',#5876,#5876,#5338,.T.);
#7146=EDGE_CURVE('',#5876,#5875,#3132,.T.);
#7147=EDGE_CURVE('',#5877,#5877,#5339,.T.);
#7148=EDGE_CURVE('',#5877,#5876,#3133,.T.);
#7149=EDGE_CURVE('',#5878,#5878,#5340,.T.);
#7150=EDGE_CURVE('',#5879,#5879,#5341,.F.);
#7151=EDGE_CURVE('',#5879,#5878,#3134,.T.);
#7152=EDGE_CURVE('',#5880,#5880,#5342,.F.);
#7153=EDGE_CURVE('',#5880,#5879,#3135,.T.);
#7154=EDGE_CURVE('',#5881,#5881,#5343,.T.);
#7155=EDGE_CURVE('',#5881,#5880,#3136,.T.);
#7156=EDGE_CURVE('',#5882,#5883,#3137,.T.);
#7157=EDGE_CURVE('',#5883,#5884,#3138,.T.);
#7158=EDGE_CURVE('',#5884,#5885,#3139,.T.);
#7159=EDGE_CURVE('',#5882,#5885,#3140,.T.);
#7160=EDGE_CURVE('',#5883,#5886,#3141,.T.);
#7161=EDGE_CURVE('',#5886,#5887,#3142,.T.);
#7162=EDGE_CURVE('',#5887,#5884,#3143,.T.);
#7163=EDGE_CURVE('',#5886,#5888,#3144,.T.);
#7164=EDGE_CURVE('',#5888,#5889,#3145,.T.);
#7165=EDGE_CURVE('',#5889,#5887,#3146,.T.);
#7166=EDGE_CURVE('',#5888,#5890,#3147,.T.);
#7167=EDGE_CURVE('',#5890,#5891,#3148,.T.);
#7168=EDGE_CURVE('',#5891,#5889,#3149,.T.);
#7169=EDGE_CURVE('',#5890,#5892,#3150,.T.);
#7170=EDGE_CURVE('',#5892,#5893,#3151,.T.);
#7171=EDGE_CURVE('',#5893,#5891,#3152,.T.);
#7172=EDGE_CURVE('',#5892,#5882,#3153,.T.);
#7173=EDGE_CURVE('',#5885,#5893,#3154,.T.);
#9278=ORIENTED_EDGE('',*,*,#7142,.F.);
#9279=ORIENTED_EDGE('',*,*,#7143,.F.);
#9280=ORIENTED_EDGE('',*,*,#7144,.T.);
#9281=ORIENTED_EDGE('',*,*,#7142,.T.);
#9282=ORIENTED_EDGE('',*,*,#7144,.F.);
#9283=ORIENTED_EDGE('',*,*,#7145,.F.);
#9284=ORIENTED_EDGE('',*,*,#7146,.T.);
#9285=ORIENTED_EDGE('',*,*,#7143,.T.);
#9286=ORIENTED_EDGE('',*,*,#7146,.F.);
#9287=ORIENTED_EDGE('',*,*,#7147,.F.);
#9288=ORIENTED_EDGE('',*,*,#7148,.T.);
#9289=ORIENTED_EDGE('',*,*,#7145,.T.);
#9290=ORIENTED_EDGE('',*,*,#7148,.F.);
#9291=ORIENTED_EDGE('',*,*,#7147,.T.);
#9292=ORIENTED_EDGE('',*,*,#7149,.F.);
#9293=ORIENTED_EDGE('',*,*,#7150,.F.);
#9294=ORIENTED_EDGE('',*,*,#7151,.T.);
#9295=ORIENTED_EDGE('',*,*,#7149,.T.);
#9296=ORIENTED_EDGE('',*,*,#7151,.F.);
#9297=ORIENTED_EDGE('',*,*,#7152,.F.);
#9298=ORIENTED_EDGE('',*,*,#7153,.T.);
#9299=ORIENTED_EDGE('',*,*,#7150,.T.);
#9300=ORIENTED_EDGE('',*,*,#7153,.F.);
#9301=ORIENTED_EDGE('',*,*,#7154,.F.);
#9302=ORIENTED_EDGE('',*,*,#7155,.T.);
#9303=ORIENTED_EDGE('',*,*,#7152,.T.);
#9304=ORIENTED_EDGE('',*,*,#7155,.F.);
#9305=ORIENTED_EDGE('',*,*,#7154,.T.);
#9306=ORIENTED_EDGE('',*,*,#7156,.T.);
#9307=ORIENTED_EDGE('',*,*,#7157,.T.);
#9308=ORIENTED_EDGE('',*,*,#7158,.T.);
#9309=ORIENTED_EDGE('',*,*,#7159,.F.);
#9310=ORIENTED_EDGE('',*,*,#7160,.T.);
#9311=ORIENTED_EDGE('',*,*,#7161,.T.);
#9312=ORIENTED_EDGE('',*,*,#7162,.T.);
#9313=ORIENTED_EDGE('',*,*,#7157,.F.);
#9314=ORIENTED_EDGE('',*,*,#7163,.T.);
#9315=ORIENTED_EDGE('',*,*,#7164,.T.);
#9316=ORIENTED_EDGE('',*,*,#7165,.T.);
#9317=ORIENTED_EDGE('',*,*,#7161,.F.);
#9318=ORIENTED_EDGE('',*,*,#7166,.T.);
#9319=ORIENTED_EDGE('',*,*,#7167,.T.);
#9320=ORIENTED_EDGE('',*,*,#7168,.T.);
#9321=ORIENTED_EDGE('',*,*,#7164,.F.);
#9322=ORIENTED_EDGE('',*,*,#7169,.T.);
#9323=ORIENTED_EDGE('',*,*,#7170,.T.);
#9324=ORIENTED_EDGE('',*,*,#7171,.T.);
#9325=ORIENTED_EDGE('',*,*,#7167,.F.);
#9326=ORIENTED_EDGE('',*,*,#7172,.T.);
#9327=ORIENTED_EDGE('',*,*,#7159,.T.);
#9328=ORIENTED_EDGE('',*,*,#7173,.T.);
#9329=ORIENTED_EDGE('',*,*,#7170,.F.);
#9330=ORIENTED_EDGE('',*,*,#7172,.F.);
#9331=ORIENTED_EDGE('',*,*,#7169,.F.);
#9332=ORIENTED_EDGE('',*,*,#7166,.F.);
#9333=ORIENTED_EDGE('',*,*,#7163,.F.);
#9334=ORIENTED_EDGE('',*,*,#7160,.F.);
#9335=ORIENTED_EDGE('',*,*,#7156,.F.);
#9336=ORIENTED_EDGE('',*,*,#7173,.F.);
#9337=ORIENTED_EDGE('',*,*,#7158,.F.);
#9338=ORIENTED_EDGE('',*,*,#7162,.F.);
#9339=ORIENTED_EDGE('',*,*,#7165,.F.);
#9340=ORIENTED_EDGE('',*,*,#7168,.F.);
#9341=ORIENTED_EDGE('',*,*,#7171,.F.);
#11727=CYLINDRICAL_SURFACE('',#13393,0.425);
#11728=CYLINDRICAL_SURFACE('',#13401,0.24505);
#12004=ADVANCED_FACE('',(#1495),#966,.T.);
#12005=ADVANCED_FACE('',(#1496),#477,.T.);
#12006=ADVANCED_FACE('',(#1497),#11727,.T.);
#12007=ADVANCED_FACE('',(#1498),#478,.T.);
#12008=ADVANCED_FACE('',(#1499,#801),#967,.T.);
#12009=ADVANCED_FACE('',(#1500),#479,.T.);
#12010=ADVANCED_FACE('',(#1501),#11728,.T.);
#12011=ADVANCED_FACE('',(#1502),#480,.T.);
#12012=ADVANCED_FACE('',(#1503),#968,.T.);
#12013=ADVANCED_FACE('',(#1504),#969,.F.);
#12014=ADVANCED_FACE('',(#1505),#970,.F.);
#12015=ADVANCED_FACE('',(#1506),#971,.F.);
#12016=ADVANCED_FACE('',(#1507),#972,.F.);
#12017=ADVANCED_FACE('',(#1508),#973,.F.);
#12018=ADVANCED_FACE('',(#1509),#974,.F.);
#12019=ADVANCED_FACE('',(#1510),#975,.F.);
#12020=ADVANCED_FACE('',(#1511),#976,.F.);
#12498=CLOSED_SHELL('',(#12004,#12005,#12006,#12007,#12008,#12009,#12010,
#12011,#12012));
#12499=CLOSED_SHELL('',(#12013,#12014,#12015,#12016,#12017,#12018,#12019,
#12020));
#13388=AXIS2_PLACEMENT_3D('',#18652,#15240,#15241);
#13389=AXIS2_PLACEMENT_3D('',#18653,#15242,#15243);
#13390=AXIS2_PLACEMENT_3D('',#18655,#15244,#15245);
#13391=AXIS2_PLACEMENT_3D('',#18656,#15246,#15247);
#13392=AXIS2_PLACEMENT_3D('',#18658,#15248,#15249);
#13393=AXIS2_PLACEMENT_3D('',#18660,#15251,#15252);
#13394=AXIS2_PLACEMENT_3D('',#18662,#15253,#15254);
#13395=AXIS2_PLACEMENT_3D('',#18664,#15256,#15257);
#13396=AXIS2_PLACEMENT_3D('',#18666,#15258,#15259);
#13397=AXIS2_PLACEMENT_3D('',#18668,#15261,#15262);
#13398=AXIS2_PLACEMENT_3D('',#18670,#15263,#15264);
#13399=AXIS2_PLACEMENT_3D('',#18671,#15265,#15266);
#13400=AXIS2_PLACEMENT_3D('',#18673,#15267,#15268);
#13401=AXIS2_PLACEMENT_3D('',#18675,#15270,#15271);
#13402=AXIS2_PLACEMENT_3D('',#18677,#15272,#15273);
#13403=AXIS2_PLACEMENT_3D('',#18679,#15275,#15276);
#13404=AXIS2_PLACEMENT_3D('',#18681,#15277,#15278);
#13405=AXIS2_PLACEMENT_3D('',#18683,#15280,#15281);
#13406=AXIS2_PLACEMENT_3D('',#18684,#15282,#15283);
#13407=AXIS2_PLACEMENT_3D('',#18693,#15288,#15289);
#13408=AXIS2_PLACEMENT_3D('',#18699,#15293,#15294);
#13409=AXIS2_PLACEMENT_3D('',#18705,#15298,#15299);
#13410=AXIS2_PLACEMENT_3D('',#18711,#15303,#15304);
#13411=AXIS2_PLACEMENT_3D('',#18717,#15308,#15309);
#13412=AXIS2_PLACEMENT_3D('',#18720,#15312,#15313);
#13413=AXIS2_PLACEMENT_3D('',#18721,#15314,#15315);
#15240=DIRECTION('axis',(0.,0.,1.));
#15241=DIRECTION('refdir',(1.,0.,0.));
#15242=DIRECTION('center_axis',(0.,1.,0.));
#15243=DIRECTION('ref_axis',(0.,0.,1.));
#15244=DIRECTION('center_axis',(0.,-1.,0.));
#15245=DIRECTION('ref_axis',(1.,0.,0.));
#15246=DIRECTION('center_axis',(0.,-1.,0.));
#15247=DIRECTION('ref_axis',(1.,0.,0.));
#15248=DIRECTION('center_axis',(0.,-1.,0.));
#15249=DIRECTION('ref_axis',(1.,0.,0.));
#15250=DIRECTION('',(0.707106781186548,0.707106781186547,8.65956056235493E-17));
#15251=DIRECTION('center_axis',(0.,-1.,0.));
#15252=DIRECTION('ref_axis',(1.,0.,0.));
#15253=DIRECTION('center_axis',(0.,-1.,0.));
#15254=DIRECTION('ref_axis',(1.,0.,0.));
#15255=DIRECTION('',(0.,1.,0.));
#15256=DIRECTION('center_axis',(0.,1.,0.));
#15257=DIRECTION('ref_axis',(1.,0.,0.));
#15258=DIRECTION('center_axis',(0.,-1.,0.));
#15259=DIRECTION('ref_axis',(1.,0.,0.));
#15260=DIRECTION('',(-0.707106781186547,0.707106781186548,-8.65956056235493E-17));
#15261=DIRECTION('center_axis',(0.,-1.,0.));
#15262=DIRECTION('ref_axis',(0.,0.,-1.));
#15263=DIRECTION('center_axis',(0.,-1.,0.));
#15264=DIRECTION('ref_axis',(1.,0.,0.));
#15265=DIRECTION('center_axis',(0.,1.,0.));
#15266=DIRECTION('ref_axis',(1.,0.,0.));
#15267=DIRECTION('center_axis',(0.,1.,0.));
#15268=DIRECTION('ref_axis',(1.,0.,0.));
#15269=DIRECTION('',(-0.447213595499958,0.894427190999916,-5.47678698264203E-17));
#15270=DIRECTION('center_axis',(0.,-1.,0.));
#15271=DIRECTION('ref_axis',(1.,0.,0.));
#15272=DIRECTION('center_axis',(0.,1.,0.));
#15273=DIRECTION('ref_axis',(1.,0.,0.));
#15274=DIRECTION('',(0.,1.,0.));
#15275=DIRECTION('center_axis',(0.,1.,0.));
#15276=DIRECTION('ref_axis',(1.,0.,0.));
#15277=DIRECTION('center_axis',(0.,-1.,0.));
#15278=DIRECTION('ref_axis',(1.,0.,0.));
#15279=DIRECTION('',(-0.707106781186547,0.707106781186548,-8.65956056235493E-17));
#15280=DIRECTION('center_axis',(0.,-1.,0.));
#15281=DIRECTION('ref_axis',(0.,0.,-1.));
#15282=DIRECTION('center_axis',(0.866025403784439,0.,-0.5));
#15283=DIRECTION('ref_axis',(0.5,0.,0.866025403784439));
#15284=DIRECTION('',(-0.5,0.,-0.866025403784439));
#15285=DIRECTION('',(0.,-1.,0.));
#15286=DIRECTION('',(0.5,0.,0.866025403784439));
#15287=DIRECTION('',(0.,-1.,0.));
#15288=DIRECTION('center_axis',(1.20185167898973E-16,0.,-1.));
#15289=DIRECTION('ref_axis',(1.,0.,1.20185167898973E-16));
#15290=DIRECTION('',(-1.,0.,-1.20185167898973E-16));
#15291=DIRECTION('',(0.,-1.,0.));
#15292=DIRECTION('',(1.,0.,1.20185167898973E-16));
#15293=DIRECTION('center_axis',(-0.866025403784439,0.,-0.5));
#15294=DIRECTION('ref_axis',(0.5,0.,-0.866025403784439));
#15295=DIRECTION('',(-0.5,0.,0.866025403784439));
#15296=DIRECTION('',(0.,-1.,0.));
#15297=DIRECTION('',(0.5,0.,-0.866025403784439));
#15298=DIRECTION('center_axis',(-0.866025403784439,0.,0.5));
#15299=DIRECTION('ref_axis',(-0.5,0.,-0.866025403784439));
#15300=DIRECTION('',(0.5,0.,0.866025403784439));
#15301=DIRECTION('',(0.,-1.,0.));
#15302=DIRECTION('',(-0.5,0.,-0.866025403784439));
#15303=DIRECTION('center_axis',(-2.40370335797945E-16,0.,1.));
#15304=DIRECTION('ref_axis',(-1.,0.,-2.40370335797945E-16));
#15305=DIRECTION('',(1.,0.,2.40370335797945E-16));
#15306=DIRECTION('',(0.,-1.,0.));
#15307=DIRECTION('',(-1.,0.,-2.40370335797945E-16));
#15308=DIRECTION('center_axis',(0.866025403784439,0.,0.5));
#15309=DIRECTION('ref_axis',(-0.5,0.,0.866025403784439));
#15310=DIRECTION('',(0.5,0.,-0.866025403784439));
#15311=DIRECTION('',(-0.5,0.,0.866025403784439));
#15312=DIRECTION('center_axis',(0.,1.,0.));
#15313=DIRECTION('ref_axis',(1.,0.,0.));
#15314=DIRECTION('center_axis',(0.,-1.,0.));
#15315=DIRECTION('ref_axis',(0.,0.,-1.));
#18652=CARTESIAN_POINT('',(0.,0.,0.));
#18653=CARTESIAN_POINT('Origin',(0.375,0.5,0.));
#18654=CARTESIAN_POINT('',(-0.375,0.5,-4.59242549680257E-17));
#18655=CARTESIAN_POINT('Origin',(0.,0.5,0.));
#18656=CARTESIAN_POINT('Origin',(0.,0.475,0.));
#18657=CARTESIAN_POINT('',(-0.425,0.45,-5.20474889637625E-17));
#18658=CARTESIAN_POINT('Origin',(0.,0.45,0.));
#18659=CARTESIAN_POINT('',(-0.4,0.475,-4.89858719658941E-17));
#18660=CARTESIAN_POINT('Origin',(0.,0.24,0.));
#18661=CARTESIAN_POINT('',(-0.425,0.0299999999999998,-5.20474889637625E-17));
#18662=CARTESIAN_POINT('Origin',(0.,0.0299999999999998,0.));
#18663=CARTESIAN_POINT('',(-0.425,0.24,-5.20474889637625E-17));
#18664=CARTESIAN_POINT('Origin',(0.,0.0150000000000001,0.));
#18665=CARTESIAN_POINT('',(-0.395,4.85722573273506E-17,-4.83735485663204E-17));
#18666=CARTESIAN_POINT('Origin',(0.,0.,0.));
#18667=CARTESIAN_POINT('',(-0.41,0.0150000000000001,-5.02105187650415E-17));
#18668=CARTESIAN_POINT('Origin',(0.27,0.,0.));
#18669=CARTESIAN_POINT('',(-0.27,0.,-3.30654635769785E-17));
#18670=CARTESIAN_POINT('Origin',(0.,0.,0.));
#18671=CARTESIAN_POINT('Origin',(0.,-0.02,0.));
#18672=CARTESIAN_POINT('',(-0.24505,-0.0498999999999999,3.00099698131059E-17));
#18673=CARTESIAN_POINT('Origin',(0.,-0.0498999999999999,0.));
#18674=CARTESIAN_POINT('',(-0.26,-0.02,-3.18408167778312E-17));
#18675=CARTESIAN_POINT('Origin',(0.,-0.995,0.));
#18676=CARTESIAN_POINT('',(-0.24505,-1.95495,3.00099698131059E-17));
#18677=CARTESIAN_POINT('Origin',(0.,-1.95495,0.));
#18678=CARTESIAN_POINT('',(-0.24505,-0.995,-3.00099698131059E-17));
#18679=CARTESIAN_POINT('Origin',(0.,-1.975,0.));
#18680=CARTESIAN_POINT('',(-0.2,-2.,-2.44929359829471E-17));
#18681=CARTESIAN_POINT('Origin',(0.,-2.,0.));
#18682=CARTESIAN_POINT('',(-0.225,-1.975,-2.75545529808154E-17));
#18683=CARTESIAN_POINT('Origin',(0.,-2.,0.));
#18684=CARTESIAN_POINT('Origin',(0.115470053837925,-0.5,-0.2));
#18685=CARTESIAN_POINT('',(0.23094010767585,-0.5,0.));
#18686=CARTESIAN_POINT('',(0.115470053837925,-0.5,-0.2));
#18687=CARTESIAN_POINT('',(0.23094010767585,-0.5,0.));
#18688=CARTESIAN_POINT('',(0.115470053837925,-0.8,-0.2));
#18689=CARTESIAN_POINT('',(0.115470053837925,-0.5,-0.2));
#18690=CARTESIAN_POINT('',(0.23094010767585,-0.8,0.));
#18691=CARTESIAN_POINT('',(0.23094010767585,-0.8,0.));
#18692=CARTESIAN_POINT('',(0.23094010767585,-0.5,0.));
#18693=CARTESIAN_POINT('Origin',(-0.115470053837925,-0.5,-0.2));
#18694=CARTESIAN_POINT('',(-0.115470053837925,-0.5,-0.2));
#18695=CARTESIAN_POINT('',(0.115470053837925,-0.5,-0.2));
#18696=CARTESIAN_POINT('',(-0.115470053837925,-0.8,-0.2));
#18697=CARTESIAN_POINT('',(-0.115470053837925,-0.5,-0.2));
#18698=CARTESIAN_POINT('',(0.115470053837925,-0.8,-0.2));
#18699=CARTESIAN_POINT('Origin',(-0.23094010767585,-0.5,-2.77555756156289E-17));
#18700=CARTESIAN_POINT('',(-0.23094010767585,-0.5,-2.82820063659975E-17));
#18701=CARTESIAN_POINT('',(-0.115470053837925,-0.5,-0.2));
#18702=CARTESIAN_POINT('',(-0.23094010767585,-0.8,-2.77555756156289E-17));
#18703=CARTESIAN_POINT('',(-0.23094010767585,-0.5,-2.82820063659975E-17));
#18704=CARTESIAN_POINT('',(-0.115470053837925,-0.8,-0.2));
#18705=CARTESIAN_POINT('Origin',(-0.115470053837925,-0.5,0.2));
#18706=CARTESIAN_POINT('',(-0.115470053837925,-0.5,0.2));
#18707=CARTESIAN_POINT('',(-0.23094010767585,-0.5,-2.82820063659975E-17));
#18708=CARTESIAN_POINT('',(-0.115470053837925,-0.8,0.2));
#18709=CARTESIAN_POINT('',(-0.115470053837925,-0.5,0.2));
#18710=CARTESIAN_POINT('',(-0.23094010767585,-0.8,-2.82820063659975E-17));
#18711=CARTESIAN_POINT('Origin',(0.115470053837925,-0.5,0.2));
#18712=CARTESIAN_POINT('',(0.115470053837925,-0.5,0.2));
#18713=CARTESIAN_POINT('',(-0.115470053837925,-0.5,0.2));
#18714=CARTESIAN_POINT('',(0.115470053837925,-0.8,0.2));
#18715=CARTESIAN_POINT('',(0.115470053837925,-0.5,0.2));
#18716=CARTESIAN_POINT('',(-0.115470053837925,-0.8,0.2));
#18717=CARTESIAN_POINT('Origin',(0.23094010767585,-0.5,0.));
#18718=CARTESIAN_POINT('',(0.115470053837925,-0.5,0.2));
#18719=CARTESIAN_POINT('',(0.115470053837925,-0.8,0.2));
#18720=CARTESIAN_POINT('Origin',(0.,-0.5,0.));
#18721=CARTESIAN_POINT('Origin',(0.,-0.8,0.));
#32671=UNCERTAINTY_MEASURE_WITH_UNIT(LENGTH_MEASURE(0.001),#32752,
'DISTANCE_ACCURACY_VALUE',
'Maximum model space distance between geometric entities at asserted c
onnectivities');
#32702=UNCERTAINTY_MEASURE_WITH_UNIT(LENGTH_MEASURE(0.001),#32752,
'DISTANCE_ACCURACY_VALUE',
'Maximum model space distance between geometric entities at asserted c
onnectivities');
#32720=(
GEOMETRIC_REPRESENTATION_CONTEXT(3)
GLOBAL_UNCERTAINTY_ASSIGNED_CONTEXT((#32671))
GLOBAL_UNIT_ASSIGNED_CONTEXT((#32752,#32754,#32755))
REPRESENTATION_CONTEXT('','3D')
);
#32751=(
GEOMETRIC_REPRESENTATION_CONTEXT(3)
GLOBAL_UNCERTAINTY_ASSIGNED_CONTEXT((#32702))
GLOBAL_UNIT_ASSIGNED_CONTEXT((#32752,#32754,#32755))
REPRESENTATION_CONTEXT('','3D')
);
#32752=(
LENGTH_UNIT()
NAMED_UNIT(*)
SI_UNIT(.CENTI.,.METRE.)
);
#32754=(
NAMED_UNIT(*)
PLANE_ANGLE_UNIT()
SI_UNIT($,.RADIAN.)
);
#32755=(
NAMED_UNIT(*)
SI_UNIT($,.STERADIAN.)
SOLID_ANGLE_UNIT()
);
#32773=SHAPE_DEFINITION_REPRESENTATION(#32821,#32946);
#32821=PRODUCT_DEFINITION_SHAPE('',$,#32995);
#32946=SHAPE_REPRESENTATION('',(#13388),#32720);
#32977=PRODUCT_DEFINITION_CONTEXT('part definition',#33123,'design');
#32995=PRODUCT_DEFINITION('Cap Screw - M5x20','Cap Screw - M5x20',#33043,
#32977);
#33043=PRODUCT_DEFINITION_FORMATION('',$,#33142);
#33123=APPLICATION_CONTEXT(
'Core Data for Automotive Mechanical Design Process');
#33124=PRODUCT_CONTEXT('part definition',#33123,'mechanical');
#33142=PRODUCT('Cap Screw - M5x20','Cap Screw - M5x20',
'Cap Screw - M5x20',(#33124));
#33243=COLOUR_RGB('Black',0.12,0.14,0.17);
#33244=FILL_AREA_STYLE_COLOUR('',#33243);
#33245=FILL_AREA_STYLE('',(#33244));
#33246=SURFACE_STYLE_FILL_AREA(#33245);
#33247=SURFACE_SIDE_STYLE('',(#33246));
#33248=SURFACE_STYLE_USAGE(.BOTH.,#33247);
#33249=PRESENTATION_STYLE_ASSIGNMENT((#33248));
ENDSEC;
END-ISO-10303-21;
